ISO-10303-21;
HEADER;
/* Generated by software containing ST-Developer
 * from STEP Tools, Inc. (www.steptools.com) 
 */

FILE_DESCRIPTION(
/* description */ ('Belt conveyor head drive unit'),
/* implementation_level */ '2;1');

FILE_NAME(
/* name */ 'Flat Washer - M8.step',
/* time_stamp */ '2026-10-28T03:26:19-07:00',
/* author */ (''),
/* organization */ (''),
/* preprocessor_version */ 'ST-DEVELOPER v20.2',
/* originating_system */ 'Autodesk Translation Framework v15.17.0.0',
/* authorisation */ '');

FILE_SCHEMA (('AUTOMOTIVE_DESIGN { 1 0 10303 214 3 1 1 }'));
ENDSEC;

DATA;
#10=MECHANICAL_DESIGN_GEOMETRIC_PRESENTATION_REPRESENTATION('',(#904),#27069);
#750=SHAPE_REPRESENTATION_RELATIONSHIP('SRR','None',#27397,#819);
#819=ADVANCED_BREP_SHAPE_REPRESENTATION('',(#987),#27039);
#904=STYLED_ITEM('',(#27804),#987);
#987=MANIFOLD_SOLID_BREP('Body1',#13771);
#1201=FACE_BOUND('',#3103,.T.);
#1202=FACE_BOUND('',#3105,.T.);
#1517=PLANE('',#15586);
#1518=PLANE('',#15587);
#2111=FACE_OUTER_BOUND('',#3100,.T.);
#2112=FACE_OUTER_BOUND('',#3101,.T.);
#2113=FACE_OUTER_BOUND('',#3102,.T.);
#2114=FACE_OUTER_BOUND('',#3104,.T.);
#3100=EDGE_LOOP('',(#11028,#11029,#11030,#11031));
#3101=EDGE_LOOP('',(#11032,#11033,#11034,#11035));
#3102=EDGE_LOOP('',(#11036));
#3103=EDGE_LOOP('',(#11037));
#3104=EDGE_LOOP('',(#11038));
#3105=EDGE_LOOP('',(#11039));
#3996=LINE('',#24298,#4788);
#3997=LINE('',#24304,#4789);
#4788=VECTOR('',#18972,0.42);
#4789=VECTOR('',#18979,0.8);
#5563=CIRCLE('',#15581,0.42);
#5564=CIRCLE('',#15582,0.42);
#5565=CIRCLE('',#15584,0.8);
#5566=CIRCLE('',#15585,0.8);
#6665=VERTEX_POINT('',#24295);
#6666=VERTEX_POINT('',#24297);
#6667=VERTEX_POINT('',#24301);
#6668=VERTEX_POINT('',#24303);
#8206=EDGE_CURVE('',#6665,#6665,#5563,.T.);
#8207=EDGE_CURVE('',#6665,#6666,#3996,.T.);
#8208=EDGE_CURVE('',#6666,#6666,#5564,.T.);
#8209=EDGE_CURVE('',#6667,#6667,#5565,.T.);
#8210=EDGE_CURVE('',#6667,#6668,#3997,.T.);
#8211=EDGE_CURVE('',#6668,#6668,#5566,.T.);
#11028=ORIENTED_EDGE('',*,*,#8206,.F.);
#11029=ORIENTED_EDGE('',*,*,#8207,.T.);
#11030=ORIENTED_EDGE('',*,*,#8208,.T.);
#11031=ORIENTED_EDGE('',*,*,#8207,.F.);
#11032=ORIENTED_EDGE('',*,*,#8209,.F.);
#11033=ORIENTED_EDGE('',*,*,#8210,.T.);
#11034=ORIENTED_EDGE('',*,*,#8211,.T.);
#11035=ORIENTED_EDGE('',*,*,#8210,.F.);
#11036=ORIENTED_EDGE('',*,*,#8209,.T.);
#11037=ORIENTED_EDGE('',*,*,#8206,.T.);
#11038=ORIENTED_EDGE('',*,*,#8211,.F.);
#11039=ORIENTED_EDGE('',*,*,#8208,.F.);
#12718=CYLINDRICAL_SURFACE('',#15580,0.42);
#12719=CYLINDRICAL_SURFACE('',#15583,0.8);
#13390=ADVANCED_FACE('',(#2111),#12718,.F.);
#13391=ADVANCED_FACE('',(#2112),#12719,.T.);
#13392=ADVANCED_FACE('',(#2113,#1201),#1517,.T.);
#13393=ADVANCED_FACE('',(#2114,#1202),#1518,.F.);
#13771=CLOSED_SHELL('',(#13390,#13391,#13392,#13393));
#15579=AXIS2_PLACEMENT_3D('',#24293,#18966,#18967);
#15580=AXIS2_PLACEMENT_3D('',#24294,#18968,#18969);
#15581=AXIS2_PLACEMENT_3D('',#24296,#18970,#18971);
#15582=AXIS2_PLACEMENT_3D('',#24299,#18973,#18974);
#15583=AXIS2_PLACEMENT_3D('',#24300,#18975,#18976);
#15584=AXIS2_PLACEMENT_3D('',#24302,#18977,#18978);
#15585=AXIS2_PLACEMENT_3D('',#24305,#18980,#18981);
#15586=AXIS2_PLACEMENT_3D('',#24306,#18982,#18983);
#15587=AXIS2_PLACEMENT_3D('',#24307,#18984,#18985);
#18966=DIRECTION('axis',(0.,0.,1.));
#18967=DIRECTION('refdir',(1.,0.,0.));
#18968=DIRECTION('center_axis',(0.,1.,0.));
#18969=DIRECTION('ref_axis',(1.,0.,0.));
#18970=DIRECTION('center_axis',(0.,-1.,0.));
#18971=DIRECTION('ref_axis',(1.,0.,0.));
#18972=DIRECTION('',(0.,-1.,0.));
#18973=DIRECTION('center_axis',(0.,-1.,0.));
#18974=DIRECTION('ref_axis',(1.,0.,0.));
#18975=DIRECTION('center_axis',(0.,1.,0.));
#18976=DIRECTION('ref_axis',(1.,0.,0.));
#18977=DIRECTION('center_axis',(0.,1.,0.));
#18978=DIRECTION('ref_axis',(1.,0.,0.));
#18979=DIRECTION('',(0.,-1.,0.));
#18980=DIRECTION('center_axis',(0.,1.,0.));
#18981=DIRECTION('ref_axis',(1.,0.,0.));
#18982=DIRECTION('center_axis',(0.,1.,0.));
#18983=DIRECTION('ref_axis',(1.,0.,0.));
#18984=DIRECTION('center_axis',(0.,1.,0.));
#18985=DIRECTION('ref_axis',(1.,0.,0.));
#24293=CARTESIAN_POINT('',(0.,0.,0.));
#24294=CARTESIAN_POINT('Origin',(0.,0.,0.));
#24295=CARTESIAN_POINT('',(-0.42,0.16,5.14351655641888E-17));
#24296=CARTESIAN_POINT('Origin',(0.,0.16,0.));
#24297=CARTESIAN_POINT('',(-0.42,0.,5.14351655641888E-17));
#24298=CARTESIAN_POINT('',(-0.42,0.,5.14351655641888E-17));
#24299=CARTESIAN_POINT('Origin',(0.,0.,0.));
#24300=CARTESIAN_POINT('Origin',(0.,0.,0.));
#24301=CARTESIAN_POINT('',(-0.8,0.16,9.79717439317883E-17));
#24302=CARTESIAN_POINT('Origin',(0.,0.16,0.));
#24303=CARTESIAN_POINT('',(-0.8,0.,9.79717439317883E-17));
#24304=CARTESIAN_POINT('',(-0.8,0.,9.79717439317883E-17));
#24305=CARTESIAN_POINT('Origin',(0.,0.,0.));
#24306=CARTESIAN_POINT('Origin',(0.,0.16,0.));
#24307=CARTESIAN_POINT('Origin',(0.,0.,0.));
#26962=UNCERTAINTY_MEASURE_WITH_UNIT(LENGTH_MEASURE(0.001),#27070,
'DISTANCE_ACCURACY_VALUE',
'Maximum model space distance between geometric entities at asserted c
onnectivities');
#26992=UNCERTAINTY_MEASURE_WITH_UNIT(LENGTH_MEASURE(0.001),#27070,
'DISTANCE_ACCURACY_VALUE',
'Maximum model space distance between geometric entities at asserted c
onnectivities');
#27039=(
GEOMETRIC_REPRESENTATION_CONTEXT(3)
GLOBAL_UNCERTAINTY_ASSIGNED_CONTEXT((#26962))
GLOBAL_UNIT_ASSIGNED_CONTEXT((#27070,#27072,#27073))
REPRESENTATION_CONTEXT('','3D')
);
#27069=(
GEOMETRIC_REPRESENTATION_CONTEXT(3)
GLOBAL_UNCERTAINTY_ASSIGNED_CONTEXT((#26992))
GLOBAL_UNIT_ASSIGNED_CONTEXT((#27070,#27072,#27073))
REPRESENTATION_CONTEXT('','3D')
);
#27070=(
LENGTH_UNIT()
NAMED_UNIT(*)
SI_UNIT(.CENTI.,.METRE.)
);
#27072=(
NAMED_UNIT(*)
PLANE_ANGLE_UNIT()
SI_UNIT($,.RADIAN.)
);
#27073=(
NAMED_UNIT(*)
SI_UNIT($,.STERADIAN.)
SOLID_ANGLE_UNIT()
);
#27120=SHAPE_DEFINITION_REPRESENTATION(#27208,#27397);
#27208=PRODUCT_DEFINITION_SHAPE('',$,#27474);
#27397=SHAPE_REPRESENTATION('',(#15579),#27039);
#27427=PRODUCT_DEFINITION_CONTEXT('part definition',#27657,'design');
#27474=PRODUCT_DEFINITION('Flat Washer - M8','Flat Washer - M8',#27550,
#27427);
#27550=PRODUCT_DEFINITION_FORMATION('',$,#27705);
#27657=APPLICATION_CONTEXT(
'Core Data for Automotive Mechanical Design Process');
#27658=PRODUCT_CONTEXT('part definition',#27657,'mechanical');
#27705=PRODUCT('Flat Washer - M8','Flat Washer - M8','Flat Washer - M8',
(#27658));
#27798=COLOUR_RGB('Black',0.12,0.14,0.17);
#27799=FILL_AREA_STYLE_COLOUR('',#27798);
#27800=FILL_AREA_STYLE('',(#27799));
#27801=SURFACE_STYLE_FILL_AREA(#27800);
#27802=SURFACE_SIDE_STYLE('',(#27801));
#27803=SURFACE_STYLE_USAGE(.BOTH.,#27802);
#27804=PRESENTATION_STYLE_ASSIGNMENT((#27803));
ENDSEC;
END-ISO-10303-21;
